ISO-10303-21;
HEADER;
FILE_DESCRIPTION (('STEP AP214'),
    '1' );
FILE_NAME ('ISO 5597-32-4-5_GB_SEALS_TYPE1 32X4X5 L1.step',
    '2026-10-08T09:53:37',
    ( '' ),
    ( '' ),
    'SwSTEP 2.0',
    'SolidWorks 2026',
    '' );
FILE_SCHEMA (( 'AUTOMOTIVE_DESIGN' ));
ENDSEC;

DATA;
#372=( NAMED_UNIT ( * ) SI_UNIT ( $, .STERADIAN. ) SOLID_ANGLE_UNIT ( ) );
#396=DIRECTION ( 'NONE',  ( -0.000000000000000000, -0.000000000000000000, 1.000000000000000000 ) ) ;
#509=ORIENTED_EDGE ( 'NONE', *, *, #24768, .F. ) ;
#1110=CIRCLE ( 'NONE', #14248, 15.50000000000000000 ) ;
#1218=CARTESIAN_POINT ( 'NONE',  ( 12.83284365640956182, 1.604257322819167057E-15, 0.000000000000000000 ) ) ;
#1953=CIRCLE ( 'NONE', #48702, 13.36666666666666536 ) ;
#2024=CARTESIAN_POINT ( 'NONE',  ( 0.000000000000000000, 0.000000000000000000, -4.400000000000001243 ) ) ;
#2110=AXIS2_PLACEMENT_3D ( 'NONE', #38774, #4210, #10194 ) ;
#2310=AXIS2_PLACEMENT_3D ( 'NONE', #38860, #55408, #3931 ) ;
#2865=EDGE_CURVE ( 'NONE', #57786, #15718, #41784, .T. ) ;
#3221=DIRECTION ( 'NONE',  ( 0.000000000000000000, 0.000000000000000000, 1.000000000000000000 ) ) ;
#3235=DIRECTION ( 'NONE',  ( -1.000000000000000000, 0.000000000000000000, 0.000000000000000000 ) ) ;
#3847=CARTESIAN_POINT ( 'NONE',  ( -15.50000000000000000, 1.898202538678397557E-15, -4.400000000000001243 ) ) ;
#3931=DIRECTION ( 'NONE',  ( -1.000000000000000000, 0.000000000000000000, 0.000000000000000000 ) ) ;
#3956=FACE_BOUND ( 'NONE', #21147, .T. ) ;
#4085=DIRECTION ( 'NONE',  ( -1.000000000000000000, 0.000000000000000000, 0.000000000000000000 ) ) ;
#4129=ADVANCED_BREP_SHAPE_REPRESENTATION ( '', ( #12047, #43395 ), #72282 ) ;
#4210=DIRECTION ( 'NONE',  ( -0.000000000000000000, -0.000000000000000000, -1.000000000000000000 ) ) ;
#4459=( LENGTH_UNIT ( ) NAMED_UNIT ( * ) SI_UNIT ( .MILLI., .METRE. ) );
#4545=CONICAL_SURFACE ( 'NONE', #57339, 14.53333333333331545, 0.3490658503988688377 ) ;
#4555=DIRECTION ( 'NONE',  ( -0.000000000000000000, -0.000000000000000000, -1.000000000000000000 ) ) ;
#4583=DIRECTION ( 'NONE',  ( -0.000000000000000000, 0.000000000000000000, 1.000000000000000000 ) ) ;
#4731=VERTEX_POINT ( 'NONE', #45081 ) ;
#4747=CARTESIAN_POINT ( 'NONE',  ( -12.50000000000000000, 1.530808498934191521E-15, -4.400000000000001243 ) ) ;
#4791=DIRECTION ( 'NONE',  ( 1.000000000000000000, 0.000000000000000000, 0.000000000000000000 ) ) ;
#4882=SURFACE_STYLE_FILL_AREA ( #17249 ) ;
#4913=FACE_OUTER_BOUND ( 'NONE', #54628, .T. ) ;
#4991=CIRCLE ( 'NONE', #6226, 15.50000000000000000 ) ;
#5040=FACE_BOUND ( 'NONE', #44481, .T. ) ;
#5129=EDGE_CURVE ( 'NONE', #41007, #12200, #1953, .T. ) ;
#5397=EDGE_CURVE ( 'NONE', #69906, #25992, #17531, .T. ) ;
#5552=EDGE_CURVE ( 'NONE', #34058, #11494, #72778, .T. ) ;
#5637=EDGE_LOOP ( 'NONE', ( #34303, #46688, #56962, #69376 ) ) ;
#6218=ORIENTED_EDGE ( 'NONE', *, *, #25806, .F. ) ;
#6226=AXIS2_PLACEMENT_3D ( 'NONE', #24655, #47586, #41955 ) ;
#6415=VERTEX_POINT ( 'NONE', #25108 ) ;
#6592=APPLICATION_CONTEXT ( 'automotive_design' ) ;
#6715=EDGE_CURVE ( 'NONE', #69906, #41007, #22437, .T. ) ;
#7211=AXIS2_PLACEMENT_3D ( 'NONE', #13163, #30812, #47388 ) ;
#7237=CIRCLE ( 'NONE', #69644, 14.53333333333331545 ) ;
#7490=ORIENTED_EDGE ( 'NONE', *, *, #40224, .F. ) ;
#7946=ORIENTED_EDGE ( 'NONE', *, *, #33077, .T. ) ;
#8564=APPLICATION_CONTEXT ( 'automotive_design' ) ;
#8641=DIRECTION ( 'NONE',  ( 1.000000000000000000, 0.000000000000000000, 0.000000000000000000 ) ) ;
#9001=FACE_OUTER_BOUND ( 'NONE', #51790, .T. ) ;
#9136=EDGE_CURVE ( 'NONE', #34500, #4731, #32473, .T. ) ;
#9573=CARTESIAN_POINT ( 'NONE',  ( 12.19999999999998863, 0.000000000000000000, -4.400000000000001243 ) ) ;
#9978=VERTEX_POINT ( 'NONE', #36958 ) ;
#10194=DIRECTION ( 'NONE',  ( -1.000000000000000000, 0.000000000000000000, 0.000000000000000000 ) ) ;
#10359=DIRECTION ( 'NONE',  ( -0.000000000000000000, -0.000000000000000000, -1.000000000000000000 ) ) ;
#10443=( NAMED_UNIT ( * ) PLANE_ANGLE_UNIT ( ) SI_UNIT ( $, .RADIAN. ) );
#10524=DIRECTION ( 'NONE',  ( -0.000000000000000000, -0.000000000000000000, 1.000000000000000000 ) ) ;
#10856=ORIENTED_EDGE ( 'NONE', *, *, #66390, .F. ) ;
#11132=EDGE_LOOP ( 'NONE', ( #64907, #43086, #70338, #28440 ) ) ;
#11494=VERTEX_POINT ( 'NONE', #3847 ) ;
#11548=SHAPE_REPRESENTATION_RELATIONSHIP ( 'NONE' , 'NONE' ,  #51769, #4129 ) ;
#11779=AXIS2_PLACEMENT_3D ( 'NONE', #23194, #39749, #22449 ) ;
#11854=ADVANCED_FACE ( 'NONE', ( #15010 ), #21377, .F. ) ;
#12047=MANIFOLD_SOLID_BREP ( 'Cut-Extrude1', #22384 ) ;
#12145=CARTESIAN_POINT ( 'NONE',  ( 0.000000000000000000, 0.000000000000000000, 0.000000000000000000 ) ) ;
#12200=VERTEX_POINT ( 'NONE', #15294 ) ;
#12560=ORIENTED_EDGE ( 'NONE', *, *, #37881, .F. ) ;
#13163=CARTESIAN_POINT ( 'NONE',  ( 0.000000000000000000, 0.000000000000000000, 0.000000000000000000 ) ) ;
#13330=ORIENTED_EDGE ( 'NONE', *, *, #17986, .F. ) ;
#14248=AXIS2_PLACEMENT_3D ( 'NONE', #23676, #46610, #69542 ) ;
#14543=PRODUCT ( 'ISO 5597-32-4-5_GB_SEALS_TYPE1 32X4X5 L1', 'ISO 5597-32-4-5_GB_SEALS_TYPE1 32X4X5 L1', '', ( #22675 ) ) ;
#14562=CYLINDRICAL_SURFACE ( 'NONE', #44185, 15.50000000000000000 ) ;
#14870=AXIS2_PLACEMENT_3D ( 'NONE', #37640, #32710, #60932 ) ;
#15010=FACE_OUTER_BOUND ( 'NONE', #5637, .T. ) ;
#15294=CARTESIAN_POINT ( 'NONE',  ( -13.36666666666666536, 0.000000000000000000, -1.466666666666671670 ) ) ;
#15718=VERTEX_POINT ( 'NONE', #71259 ) ;
#15757=MECHANICAL_DESIGN_GEOMETRIC_PRESENTATION_REPRESENTATION('',(#61378),#38562);
#16084=CARTESIAN_POINT ( 'NONE',  ( 0.000000000000000000, 0.000000000000000000, 0.000000000000000000 ) ) ;
#16211=DIRECTION ( 'NONE',  ( 1.000000000000000000, 0.000000000000000000, 0.000000000000000000 ) ) ;
#16312=ORIENTED_EDGE ( 'NONE', *, *, #34453, .F. ) ;
#16409=ORIENTED_EDGE ( 'NONE', *, *, #34453, .T. ) ;
#17249=FILL_AREA_STYLE ('',( #22902 ) ) ;
#17531=CIRCLE ( 'NONE', #60741, 12.83284365640956182 ) ;
#17539=CIRCLE ( 'NONE', #51181, 15.06715634359041900 ) ;
#17668=CARTESIAN_POINT ( 'NONE',  ( -14.53333333333331545, 1.812507246801946101E-15, -1.466666666666671670 ) ) ;
#17833=EDGE_LOOP ( 'NONE', ( #25458, #67095 ) ) ;
#17862=EDGE_LOOP ( 'NONE', ( #26155, #58949 ) ) ;
#17986=EDGE_CURVE ( 'NONE', #34058, #49826, #29768, .T. ) ;
#18008=DIRECTION ( 'NONE',  ( 1.000000000000000000, 0.000000000000000000, 0.000000000000000000 ) ) ;
#18024=ORIENTED_EDGE ( 'NONE', *, *, #35816, .T. ) ;
#18052=ORIENTED_EDGE ( 'NONE', *, *, #6715, .T. ) ;
#18620=CIRCLE ( 'NONE', #60658, 13.36666666666666536 ) ;
#18724=EDGE_CURVE ( 'NONE', #15718, #57786, #69062, .T. ) ;
#18901=CONICAL_SURFACE ( 'NONE', #2110, 12.83284365640956182, 0.3490658503988688377 ) ;
#18931=ORIENTED_EDGE ( 'NONE', *, *, #5129, .T. ) ;
#19449=CIRCLE ( 'NONE', #20638, 15.50000000000000000 ) ;
#19465=ADVANCED_FACE ( 'NONE', ( #4913 ), #27813, .T. ) ;
#19735=DIRECTION ( 'NONE',  ( 1.000000000000000000, 0.000000000000000000, 0.000000000000000000 ) ) ;
#19864=( LENGTH_UNIT ( ) NAMED_UNIT ( * ) SI_UNIT ( .MILLI., .METRE. ) );
#20319=DIRECTION ( 'NONE',  ( -1.000000000000000000, 0.000000000000000000, 0.000000000000000000 ) ) ;
#20638=AXIS2_PLACEMENT_3D ( 'NONE', #21852, #4583, #16211 ) ;
#20659=DIRECTION ( 'NONE',  ( 1.000000000000000000, 0.000000000000000000, 0.000000000000000000 ) ) ;
#20953=AXIS2_PLACEMENT_3D ( 'NONE', #27434, #44752, #33443 ) ;
#21147=EDGE_LOOP ( 'NONE', ( #31466, #33559 ) ) ;
#21217=FACE_BOUND ( 'NONE', #50736, .T. ) ;
#21377=CYLINDRICAL_SURFACE ( 'NONE', #73316, 12.50000000000000000 ) ;
#21405=DIRECTION ( 'NONE',  ( -0.000000000000000000, 0.000000000000000000, 1.000000000000000000 ) ) ;
#21852=CARTESIAN_POINT ( 'NONE',  ( 0.000000000000000000, 0.000000000000000000, 0.000000000000000000 ) ) ;
#22328=CARTESIAN_POINT ( 'NONE',  ( 0.000000000000000000, 0.000000000000000000, -1.466666666666671670 ) ) ;
#22384=CLOSED_SHELL ( 'NONE', ( #52970, #29434, #27739, #33497, #27243, #63273, #55083, #67379, #35833, #19465, #42601, #11854 ) ) ;
#22428=FACE_OUTER_BOUND ( 'NONE', #69702, .T. ) ;
#22437=LINE ( 'NONE', #29167, #44822 ) ;
#22449=DIRECTION ( 'NONE',  ( 1.000000000000000000, 0.000000000000000000, 0.000000000000000000 ) ) ;
#22675=PRODUCT_CONTEXT ( 'NONE', #6592, 'mechanical' ) ;
#22831=DIRECTION ( 'NONE',  ( -0.3420201433256714330, 4.188538737677025045E-17, 0.9396926207859073177 ) ) ;
#22902=FILL_AREA_STYLE_COLOUR ( '', #64981 ) ;
#23054=DIRECTION ( 'NONE',  ( -0.000000000000000000, -0.000000000000000000, 1.000000000000000000 ) ) ;
#23194=CARTESIAN_POINT ( 'NONE',  ( 0.000000000000000000, 0.000000000000000000, 0.000000000000000000 ) ) ;
#23309=UNCERTAINTY_MEASURE_WITH_UNIT (LENGTH_MEASURE( 1.000000000000000082E-05 ), #52190, 'distance_accuracy_value', 'NONE');
#23676=CARTESIAN_POINT ( 'NONE',  ( 0.000000000000000000, 0.000000000000000000, 0.000000000000000000 ) ) ;
#23779=LINE ( 'NONE', #57260, #41560 ) ;
#24655=CARTESIAN_POINT ( 'NONE',  ( 0.000000000000000000, 0.000000000000000000, -4.400000000000001243 ) ) ;
#24768=EDGE_CURVE ( 'NONE', #50378, #6415, #47299, .T. ) ;
#24909=DIRECTION ( 'NONE',  ( 1.000000000000000000, 0.000000000000000000, 0.000000000000000000 ) ) ;
#25108=CARTESIAN_POINT ( 'NONE',  ( 15.06715634359041900, 0.000000000000000000, 0.000000000000000000 ) ) ;
#25371=ORIENTED_EDGE ( 'NONE', *, *, #37881, .T. ) ;
#25458=ORIENTED_EDGE ( 'NONE', *, *, #40224, .T. ) ;
#25493=COLOUR_RGB ( '', 0.66274510, 0.83137255, 0.94901961) ;
#25750=VECTOR ( 'NONE', #23054, 1000.000000000000000 ) ;
#25806=EDGE_CURVE ( 'NONE', #12200, #41007, #18620, .T. ) ;
#25851=AXIS2_PLACEMENT_3D ( 'NONE', #9573, #3221, #43442 ) ;
#25874=ORIENTED_EDGE ( 'NONE', *, *, #24768, .T. ) ;
#25992=VERTEX_POINT ( 'NONE', #30243 ) ;
#26127=ORIENTED_EDGE ( 'NONE', *, *, #44908, .F. ) ;
#26155=ORIENTED_EDGE ( 'NONE', *, *, #71795, .F. ) ;
#26319=DIRECTION ( 'NONE',  ( -0.000000000000000000, 0.000000000000000000, 1.000000000000000000 ) ) ;
#26381=ORIENTED_EDGE ( 'NONE', *, *, #33077, .F. ) ;
#26389=EDGE_CURVE ( 'NONE', #9978, #57786, #23779, .T. ) ;
#26656=DIRECTION ( 'NONE',  ( 0.000000000000000000, 0.000000000000000000, 1.000000000000000000 ) ) ;
#26828=PLANE ( 'NONE',  #2310 ) ;
#26882=ORIENTED_EDGE ( 'NONE', *, *, #9136, .T. ) ;
#26980=DIRECTION ( 'NONE',  ( -0.000000000000000000, -0.000000000000000000, -1.000000000000000000 ) ) ;
#27019=CARTESIAN_POINT ( 'NONE',  ( 0.000000000000000000, 0.000000000000000000, -1.466666666666671670 ) ) ;
#27049=CARTESIAN_POINT ( 'NONE',  ( 0.000000000000000000, 0.000000000000000000, -4.400000000000001243 ) ) ;
#27243=ADVANCED_FACE ( 'NONE', ( #72230 ), #18901, .T. ) ;
#27434=CARTESIAN_POINT ( 'NONE',  ( 0.000000000000000000, 0.000000000000000000, -4.400000000000001243 ) ) ;
#27739=ADVANCED_FACE ( 'NONE', ( #9001 ), #4545, .F. ) ;
#27783=( NAMED_UNIT ( * ) PLANE_ANGLE_UNIT ( ) SI_UNIT ( $, .RADIAN. ) );
#27813=CYLINDRICAL_SURFACE ( 'NONE', #20953, 15.50000000000000000 ) ;
#27945=FACE_OUTER_BOUND ( 'NONE', #17862, .T. ) ;
#28034=CARTESIAN_POINT ( 'NONE',  ( 0.000000000000000000, 0.000000000000000000, 0.000000000000000000 ) ) ;
#28104=SURFACE_SIDE_STYLE ('',( #32994 ) ) ;
#28358=AXIS2_PLACEMENT_3D ( 'NONE', #2024, #54239, #24909 ) ;
#28440=ORIENTED_EDGE ( 'NONE', *, *, #26389, .F. ) ;
#29167=CARTESIAN_POINT ( 'NONE',  ( 12.83284365640956182, 1.571570090778038719E-15, 0.000000000000000000 ) ) ;
#29434=ADVANCED_FACE ( 'NONE', ( #66092 ), #14562, .T. ) ;
#29496=DIRECTION ( 'NONE',  ( -1.000000000000000000, 0.000000000000000000, 0.000000000000000000 ) ) ;
#29657=ORIENTED_EDGE ( 'NONE', *, *, #44908, .T. ) ;
#29768=LINE ( 'NONE', #69274, #25750 ) ;
#30243=CARTESIAN_POINT ( 'NONE',  ( -12.83284365640956182, 0.000000000000000000, 0.000000000000000000 ) ) ;
#30589=CIRCLE ( 'NONE', #66624, 12.50000000000000000 ) ;
#30812=DIRECTION ( 'NONE',  ( -0.000000000000000000, -0.000000000000000000, -1.000000000000000000 ) ) ;
#31466=ORIENTED_EDGE ( 'NONE', *, *, #52819, .T. ) ;
#31611=ORIENTED_EDGE ( 'NONE', *, *, #5129, .F. ) ;
#31788=AXIS2_PLACEMENT_3D ( 'NONE', #28034, #50975, #68276 ) ;
#32064=EDGE_LOOP ( 'NONE', ( #45502, #69336 ) ) ;
#32353=DIRECTION ( 'NONE',  ( -1.000000000000000000, 0.000000000000000000, 0.000000000000000000 ) ) ;
#32473=CIRCLE ( 'NONE', #68506, 14.53333333333331545 ) ;
#32710=DIRECTION ( 'NONE',  ( -0.000000000000000000, -0.000000000000000000, -1.000000000000000000 ) ) ;
#32994=SURFACE_STYLE_FILL_AREA ( #63093 ) ;
#33077=EDGE_CURVE ( 'NONE', #11494, #73475, #56780, .T. ) ;
#33197=LINE ( 'NONE', #44504, #34818 ) ;
#33299=CARTESIAN_POINT ( 'NONE',  ( 13.36666666666666536, 1.636944554860295198E-15, -1.466666666666671670 ) ) ;
#33336=CARTESIAN_POINT ( 'NONE',  ( -14.53333333333331545, 1.779820014760817565E-15, -1.466666666666671670 ) ) ;
#33443=DIRECTION ( 'NONE',  ( 1.000000000000000000, 0.000000000000000000, 0.000000000000000000 ) ) ;
#33497=ADVANCED_FACE ( 'NONE', ( #66846 ), #64776, .T. ) ;
#33559=ORIENTED_EDGE ( 'NONE', *, *, #52728, .T. ) ;
#33595=DIRECTION ( 'NONE',  ( -1.000000000000000000, 0.000000000000000000, 0.000000000000000000 ) ) ;
#33755=EDGE_LOOP ( 'NONE', ( #68509, #18931 ) ) ;
#34058=VERTEX_POINT ( 'NONE', #45610 ) ;
#34195=ORIENTED_EDGE ( 'NONE', *, *, #9136, .F. ) ;
#34303=ORIENTED_EDGE ( 'NONE', *, *, #58654, .F. ) ;
#34453=EDGE_CURVE ( 'NONE', #4731, #34500, #7237, .T. ) ;
#34500=VERTEX_POINT ( 'NONE', #17668 ) ;
#34613=DIRECTION ( 'NONE',  ( 0.3420201433256714330, 0.000000000000000000, 0.9396926207859073177 ) ) ;
#34818=VECTOR ( 'NONE', #56528, 1000.000000000000114 ) ;
#35452=DIRECTION ( 'NONE',  ( -0.000000000000000000, -0.000000000000000000, -1.000000000000000000 ) ) ;
#35816=EDGE_CURVE ( 'NONE', #11494, #34058, #4991, .T. ) ;
#35833=ADVANCED_FACE ( 'NONE', ( #21217, #55073 ), #60364, .F. ) ;
#35883=FACE_OUTER_BOUND ( 'NONE', #48571, .T. ) ;
#36381=PRODUCT_DEFINITION_FORMATION_WITH_SPECIFIED_SOURCE ( 'ANY', '', #14543, .NOT_KNOWN. ) ;
#36607=AXIS2_PLACEMENT_3D ( 'NONE', #27049, #26319, #62416 ) ;
#36958=CARTESIAN_POINT ( 'NONE',  ( 12.50000000000000000, 0.000000000000000000, -4.400000000000001243 ) ) ;
#37640=CARTESIAN_POINT ( 'NONE',  ( 0.000000000000000000, 0.000000000000000000, 0.000000000000000000 ) ) ;
#37881=EDGE_CURVE ( 'NONE', #6415, #50378, #17539, .T. ) ;
#37978=CARTESIAN_POINT ( 'NONE',  ( 0.000000000000000000, 0.000000000000000000, -4.400000000000001243 ) ) ;
#38235=CARTESIAN_POINT ( 'NONE',  ( -12.50000000000000000, 1.530808498934191521E-15, -4.400000000000001243 ) ) ;
#38562=( GEOMETRIC_REPRESENTATION_CONTEXT ( 3 ) GLOBAL_UNCERTAINTY_ASSIGNED_CONTEXT ( ( #23309 ) ) GLOBAL_UNIT_ASSIGNED_CONTEXT ( ( #52190, #27783, #372 ) ) REPRESENTATION_CONTEXT ( 'NONE', 'WORKASPACE' ) );
#38774=CARTESIAN_POINT ( 'NONE',  ( 0.000000000000000000, 0.000000000000000000, 0.000000000000000000 ) ) ;
#38860=CARTESIAN_POINT ( 'NONE',  ( 12.02279259712643622, 0.000000000000000000, 0.000000000000000000 ) ) ;
#39351=CARTESIAN_POINT ( 'NONE',  ( 0.000000000000000000, 0.000000000000000000, -1.466666666666671670 ) ) ;
#39749=DIRECTION ( 'NONE',  ( -0.000000000000000000, 0.000000000000000000, 1.000000000000000000 ) ) ;
#39902=STYLED_ITEM ( 'NONE', ( #56701 ), #4129 ) ;
#40095=DIRECTION ( 'NONE',  ( -1.000000000000000000, 0.000000000000000000, 0.000000000000000000 ) ) ;
#40224=EDGE_CURVE ( 'NONE', #49826, #73475, #1110, .T. ) ;
#40807=FACE_BOUND ( 'NONE', #33755, .T. ) ;
#41007=VERTEX_POINT ( 'NONE', #33299 ) ;
#41074=ORIENTED_EDGE ( 'NONE', *, *, #17986, .T. ) ;
#41439=DIRECTION ( 'NONE',  ( -0.000000000000000000, -0.000000000000000000, 1.000000000000000000 ) ) ;
#41560=VECTOR ( 'NONE', #41439, 1000.000000000000000 ) ;
#41784=CIRCLE ( 'NONE', #11779, 12.50000000000000000 ) ;
#41955=DIRECTION ( 'NONE',  ( 1.000000000000000000, 0.000000000000000000, 0.000000000000000000 ) ) ;
#42467=ORIENTED_EDGE ( 'NONE', *, *, #5552, .T. ) ;
#42601=ADVANCED_FACE ( 'NONE', ( #3956, #60718 ), #61077, .F. ) ;
#42733=ORIENTED_EDGE ( 'NONE', *, *, #46456, .F. ) ;
#42903=ORIENTED_EDGE ( 'NONE', *, *, #2865, .F. ) ;
#43086=ORIENTED_EDGE ( 'NONE', *, *, #58654, .T. ) ;
#43395=AXIS2_PLACEMENT_3D ( 'NONE', #48320, #71232, #19735 ) ;
#43442=DIRECTION ( 'NONE',  ( 1.000000000000000000, 0.000000000000000000, -0.000000000000000000 ) ) ;
#43452=DIRECTION ( 'NONE',  ( -0.000000000000000000, 0.000000000000000000, -1.000000000000000000 ) ) ;
#44185=AXIS2_PLACEMENT_3D ( 'NONE', #44256, #67186, #55904 ) ;
#44256=CARTESIAN_POINT ( 'NONE',  ( 0.000000000000000000, 0.000000000000000000, -4.400000000000001243 ) ) ;
#44267=VECTOR ( 'NONE', #10524, 1000.000000000000000 ) ;
#44481=EDGE_LOOP ( 'NONE', ( #42903, #68803 ) ) ;
#44504=CARTESIAN_POINT ( 'NONE',  ( -12.83284365640956182, 0.000000000000000000, 0.000000000000000000 ) ) ;
#44589=DIRECTION ( 'NONE',  ( -0.000000000000000000, -0.000000000000000000, 1.000000000000000000 ) ) ;
#44752=DIRECTION ( 'NONE',  ( -0.000000000000000000, -0.000000000000000000, 1.000000000000000000 ) ) ;
#44822=VECTOR ( 'NONE', #69397, 1000.000000000000114 ) ;
#44908=EDGE_CURVE ( 'NONE', #34500, #50378, #56678, .T. ) ;
#45042=SURFACE_STYLE_USAGE ( .BOTH. , #28104 ) ;
#45081=CARTESIAN_POINT ( 'NONE',  ( 14.53333333333331545, 0.000000000000000000, -1.466666666666671670 ) ) ;
#45271=DIRECTION ( 'NONE',  ( -0.000000000000000000, -0.000000000000000000, -1.000000000000000000 ) ) ;
#45502=ORIENTED_EDGE ( 'NONE', *, *, #5552, .F. ) ;
#45610=CARTESIAN_POINT ( 'NONE',  ( 15.50000000000000000, 0.000000000000000000, -4.400000000000001243 ) ) ;
#46456=EDGE_CURVE ( 'NONE', #25992, #12200, #33197, .T. ) ;
#46610=DIRECTION ( 'NONE',  ( -0.000000000000000000, 0.000000000000000000, 1.000000000000000000 ) ) ;
#46688=ORIENTED_EDGE ( 'NONE', *, *, #52819, .F. ) ;
#46817=DIRECTION ( 'NONE',  ( -0.000000000000000000, 0.000000000000000000, -1.000000000000000000 ) ) ;
#47003=AXIS2_PLACEMENT_3D ( 'NONE', #54706, #43452, #3235 ) ;
#47299=CIRCLE ( 'NONE', #14870, 15.06715634359041900 ) ;
#47388=DIRECTION ( 'NONE',  ( -1.000000000000000000, 0.000000000000000000, 0.000000000000000000 ) ) ;
#47586=DIRECTION ( 'NONE',  ( -0.000000000000000000, 0.000000000000000000, 1.000000000000000000 ) ) ;
#48320=CARTESIAN_POINT ( 'NONE',  ( 0.000000000000000000, 0.000000000000000000, 0.000000000000000000 ) ) ;
#48352=EDGE_CURVE ( 'NONE', #73475, #49826, #19449, .T. ) ;
#48571=EDGE_LOOP ( 'NONE', ( #16312, #34195 ) ) ;
#48702=AXIS2_PLACEMENT_3D ( 'NONE', #22328, #45271, #33595 ) ;
#48884=CARTESIAN_POINT ( 'NONE',  ( 0.000000000000000000, 0.000000000000000000, 0.000000000000000000 ) ) ;
#49826=VERTEX_POINT ( 'NONE', #58205 ) ;
#49912=VECTOR ( 'NONE', #44589, 1000.000000000000000 ) ;
#50036=CARTESIAN_POINT ( 'NONE',  ( 14.53333333333331545, 0.000000000000000000, -1.466666666666671670 ) ) ;
#50378=VERTEX_POINT ( 'NONE', #58483 ) ;
#50736=EDGE_LOOP ( 'NONE', ( #25371, #25874 ) ) ;
#50957=DIRECTION ( 'NONE',  ( -1.000000000000000000, 0.000000000000000000, 0.000000000000000000 ) ) ;
#50975=DIRECTION ( 'NONE',  ( -0.000000000000000000, 0.000000000000000000, 1.000000000000000000 ) ) ;
#51181=AXIS2_PLACEMENT_3D ( 'NONE', #48884, #71807, #20319 ) ;
#51637=DIRECTION ( 'NONE',  ( -1.000000000000000000, 0.000000000000000000, 0.000000000000000000 ) ) ;
#51728=EDGE_LOOP ( 'NONE', ( #42467, #7946, #7490, #13330 ) ) ;
#51769=SHAPE_REPRESENTATION ( 'ISO 5597-32-4-5_GB_SEALS_TYPE1 32X4X5 L1', ( #43395 ), #72282 ) ;
#51790=EDGE_LOOP ( 'NONE', ( #16409, #29657, #12560, #10856 ) ) ;
#51851=CARTESIAN_POINT ( 'NONE',  ( 0.000000000000000000, 0.000000000000000000, -4.400000000000001243 ) ) ;
#52025=CARTESIAN_POINT ( 'NONE',  ( 12.50000000000000000, 0.000000000000000000, 0.000000000000000000 ) ) ;
#52190=( LENGTH_UNIT ( ) NAMED_UNIT ( * ) SI_UNIT ( .MILLI., .METRE. ) );
#52215=CYLINDRICAL_SURFACE ( 'NONE', #60622, 12.50000000000000000 ) ;
#52338=SHAPE_DEFINITION_REPRESENTATION ( #54771, #51769 ) ;
#52728=EDGE_CURVE ( 'NONE', #73858, #9978, #71370, .T. ) ;
#52819=EDGE_CURVE ( 'NONE', #9978, #73858, #30589, .T. ) ;
#52970=ADVANCED_FACE ( 'NONE', ( #74036 ), #52215, .F. ) ;
#53186=PLANE ( 'NONE',  #56728 ) ;
#53621=PRODUCT_DEFINITION ( 'UNKNOWN', '', #36381, #66452 ) ;
#54239=DIRECTION ( 'NONE',  ( -0.000000000000000000, 0.000000000000000000, 1.000000000000000000 ) ) ;
#54502=DIRECTION ( 'NONE',  ( -0.000000000000000000, -0.000000000000000000, 1.000000000000000000 ) ) ;
#54628=EDGE_LOOP ( 'NONE', ( #26381, #18024, #41074, #70195 ) ) ;
#54706=CARTESIAN_POINT ( 'NONE',  ( 15.87720740287354459, 0.000000000000000000, 0.000000000000000000 ) ) ;
#54771=PRODUCT_DEFINITION_SHAPE ( 'NONE', 'NONE',  #53621 ) ;
#55073=FACE_OUTER_BOUND ( 'NONE', #17833, .T. ) ;
#55083=ADVANCED_FACE ( 'NONE', ( #35883, #40807 ), #53186, .F. ) ;
#55408=DIRECTION ( 'NONE',  ( -0.000000000000000000, 0.000000000000000000, -1.000000000000000000 ) ) ;
#55506=MECHANICAL_DESIGN_GEOMETRIC_PRESENTATION_REPRESENTATION('',(#39902),#60293);
#55730=UNCERTAINTY_MEASURE_WITH_UNIT (LENGTH_MEASURE( 1.000000000000000082E-05 ), #19864, 'distance_accuracy_value', 'NONE');
#55904=DIRECTION ( 'NONE',  ( 1.000000000000000000, 0.000000000000000000, 0.000000000000000000 ) ) ;
#56036=CARTESIAN_POINT ( 'NONE',  ( 0.000000000000000000, 0.000000000000000000, -1.466666666666671670 ) ) ;
#56277=CARTESIAN_POINT ( 'NONE',  ( 0.000000000000000000, 0.000000000000000000, -1.466666666666671670 ) ) ;
#56528=DIRECTION ( 'NONE',  ( -0.3420201433256714330, 0.000000000000000000, -0.9396926207859073177 ) ) ;
#56653=DIRECTION ( 'NONE',  ( 0.000000000000000000, 0.000000000000000000, 1.000000000000000000 ) ) ;
#56678=LINE ( 'NONE', #33336, #60005 ) ;
#56701=PRESENTATION_STYLE_ASSIGNMENT (( #45042 ) ) ;
#56728=AXIS2_PLACEMENT_3D ( 'NONE', #58090, #46817, #29496 ) ;
#56780=LINE ( 'NONE', #72190, #44267 ) ;
#56962=ORIENTED_EDGE ( 'NONE', *, *, #26389, .T. ) ;
#57067=FILL_AREA_STYLE_COLOUR ( '', #25493 ) ;
#57260=CARTESIAN_POINT ( 'NONE',  ( 12.50000000000000000, 0.000000000000000000, -4.400000000000001243 ) ) ;
#57339=AXIS2_PLACEMENT_3D ( 'NONE', #27019, #26656, #8641 ) ;
#57428=( NAMED_UNIT ( * ) SI_UNIT ( $, .STERADIAN. ) SOLID_ANGLE_UNIT ( ) );
#57786=VERTEX_POINT ( 'NONE', #52025 ) ;
#58090=CARTESIAN_POINT ( 'NONE',  ( 14.53333333333331545, 0.000000000000000000, -1.466666666666671670 ) ) ;
#58160=EDGE_LOOP ( 'NONE', ( #68798, #18052, #6218, #42733 ) ) ;
#58205=CARTESIAN_POINT ( 'NONE',  ( 15.50000000000000000, 0.000000000000000000, 0.000000000000000000 ) ) ;
#58483=CARTESIAN_POINT ( 'NONE',  ( -15.06715634359041900, 1.845194478843074636E-15, 0.000000000000000000 ) ) ;
#58654=EDGE_CURVE ( 'NONE', #73858, #15718, #74250, .T. ) ;
#58949=ORIENTED_EDGE ( 'NONE', *, *, #5397, .F. ) ;
#60005=VECTOR ( 'NONE', #22831, 1000.000000000000114 ) ;
#60293=( GEOMETRIC_REPRESENTATION_CONTEXT ( 3 ) GLOBAL_UNCERTAINTY_ASSIGNED_CONTEXT ( ( #72998 ) ) GLOBAL_UNIT_ASSIGNED_CONTEXT ( ( #4459, #73591, #67966 ) ) REPRESENTATION_CONTEXT ( 'NONE', 'WORKASPACE' ) );
#60364=PLANE ( 'NONE',  #47003 ) ;
#60622=AXIS2_PLACEMENT_3D ( 'NONE', #51851, #396, #18008 ) ;
#60658=AXIS2_PLACEMENT_3D ( 'NONE', #73505, #10359, #50957 ) ;
#60718=FACE_OUTER_BOUND ( 'NONE', #32064, .T. ) ;
#60741=AXIS2_PLACEMENT_3D ( 'NONE', #12145, #35452, #51637 ) ;
#60788=ORIENTED_EDGE ( 'NONE', *, *, #5397, .T. ) ;
#60932=DIRECTION ( 'NONE',  ( -1.000000000000000000, 0.000000000000000000, 0.000000000000000000 ) ) ;
#61077=PLANE ( 'NONE',  #25851 ) ;
#61378=STYLED_ITEM ( 'NONE', ( #63136 ), #12047 ) ;
#61715=LINE ( 'NONE', #50036, #73928 ) ;
#61922=AXIS2_PLACEMENT_3D ( 'NONE', #39351, #56653, #4791 ) ;
#62416=DIRECTION ( 'NONE',  ( 1.000000000000000000, 0.000000000000000000, 0.000000000000000000 ) ) ;
#63093=FILL_AREA_STYLE ('',( #57067 ) ) ;
#63136=PRESENTATION_STYLE_ASSIGNMENT (( #74008 ) ) ;
#63273=ADVANCED_FACE ( 'NONE', ( #5040, #27945 ), #26828, .F. ) ;
#63892=EDGE_LOOP ( 'NONE', ( #73740, #60788, #73501, #31611 ) ) ;
#64776=CONICAL_SURFACE ( 'NONE', #74315, 12.83284365640956182, 0.3490658503988688377 ) ;
#64907=ORIENTED_EDGE ( 'NONE', *, *, #52728, .F. ) ;
#64981=COLOUR_RGB ( '', 0.66274510, 0.83137255, 0.94901961) ;
#66092=FACE_OUTER_BOUND ( 'NONE', #51728, .T. ) ;
#66390=EDGE_CURVE ( 'NONE', #4731, #6415, #61715, .T. ) ;
#66452=PRODUCT_DEFINITION_CONTEXT ( 'detailed design', #8564, 'design' ) ;
#66624=AXIS2_PLACEMENT_3D ( 'NONE', #37978, #21405, #67666 ) ;
#66846=FACE_OUTER_BOUND ( 'NONE', #58160, .T. ) ;
#67095=ORIENTED_EDGE ( 'NONE', *, *, #48352, .T. ) ;
#67186=DIRECTION ( 'NONE',  ( -0.000000000000000000, -0.000000000000000000, 1.000000000000000000 ) ) ;
#67379=ADVANCED_FACE ( 'NONE', ( #22428 ), #69113, .F. ) ;
#67666=DIRECTION ( 'NONE',  ( 1.000000000000000000, 0.000000000000000000, 0.000000000000000000 ) ) ;
#67966=( NAMED_UNIT ( * ) SI_UNIT ( $, .STERADIAN. ) SOLID_ANGLE_UNIT ( ) );
#68009=SURFACE_SIDE_STYLE ('',( #4882 ) ) ;
#68276=DIRECTION ( 'NONE',  ( 1.000000000000000000, 0.000000000000000000, 0.000000000000000000 ) ) ;
#68506=AXIS2_PLACEMENT_3D ( 'NONE', #56277, #73921, #40095 ) ;
#68509=ORIENTED_EDGE ( 'NONE', *, *, #25806, .T. ) ;
#68798=ORIENTED_EDGE ( 'NONE', *, *, #71795, .T. ) ;
#68803=ORIENTED_EDGE ( 'NONE', *, *, #18724, .F. ) ;
#69062=CIRCLE ( 'NONE', #31788, 12.50000000000000000 ) ;
#69113=CONICAL_SURFACE ( 'NONE', #61922, 14.53333333333331545, 0.3490658503988688377 ) ;
#69274=CARTESIAN_POINT ( 'NONE',  ( 15.50000000000000000, 0.000000000000000000, -4.400000000000001243 ) ) ;
#69336=ORIENTED_EDGE ( 'NONE', *, *, #35816, .F. ) ;
#69376=ORIENTED_EDGE ( 'NONE', *, *, #2865, .T. ) ;
#69397=DIRECTION ( 'NONE',  ( 0.3420201433256714330, 4.188538737677025045E-17, -0.9396926207859073177 ) ) ;
#69542=DIRECTION ( 'NONE',  ( 1.000000000000000000, 0.000000000000000000, 0.000000000000000000 ) ) ;
#69624=CIRCLE ( 'NONE', #7211, 12.83284365640956182 ) ;
#69644=AXIS2_PLACEMENT_3D ( 'NONE', #56036, #4555, #32353 ) ;
#69702=EDGE_LOOP ( 'NONE', ( #26127, #26882, #70436, #509 ) ) ;
#69906=VERTEX_POINT ( 'NONE', #1218 ) ;
#70195=ORIENTED_EDGE ( 'NONE', *, *, #48352, .F. ) ;
#70338=ORIENTED_EDGE ( 'NONE', *, *, #18724, .T. ) ;
#70436=ORIENTED_EDGE ( 'NONE', *, *, #66390, .T. ) ;
#71232=DIRECTION ( 'NONE',  ( 0.000000000000000000, 0.000000000000000000, 1.000000000000000000 ) ) ;
#71259=CARTESIAN_POINT ( 'NONE',  ( -12.50000000000000000, 1.530808498934191521E-15, 0.000000000000000000 ) ) ;
#71370=CIRCLE ( 'NONE', #36607, 12.50000000000000000 ) ;
#71505=CARTESIAN_POINT ( 'NONE',  ( -15.50000000000000000, 1.898202538678397557E-15, 0.000000000000000000 ) ) ;
#71795=EDGE_CURVE ( 'NONE', #25992, #69906, #69624, .T. ) ;
#71807=DIRECTION ( 'NONE',  ( -0.000000000000000000, -0.000000000000000000, -1.000000000000000000 ) ) ;
#72190=CARTESIAN_POINT ( 'NONE',  ( -15.50000000000000000, 1.898202538678397557E-15, -4.400000000000001243 ) ) ;
#72230=FACE_OUTER_BOUND ( 'NONE', #63892, .T. ) ;
#72282=( GEOMETRIC_REPRESENTATION_CONTEXT ( 3 ) GLOBAL_UNCERTAINTY_ASSIGNED_CONTEXT ( ( #55730 ) ) GLOBAL_UNIT_ASSIGNED_CONTEXT ( ( #19864, #10443, #57428 ) ) REPRESENTATION_CONTEXT ( 'NONE', 'WORKASPACE' ) );
#72516=CARTESIAN_POINT ( 'NONE',  ( 0.000000000000000000, 0.000000000000000000, -4.400000000000001243 ) ) ;
#72778=CIRCLE ( 'NONE', #28358, 15.50000000000000000 ) ;
#72998=UNCERTAINTY_MEASURE_WITH_UNIT (LENGTH_MEASURE( 1.000000000000000082E-05 ), #4459, 'distance_accuracy_value', 'NONE');
#73316=AXIS2_PLACEMENT_3D ( 'NONE', #72516, #54502, #20659 ) ;
#73475=VERTEX_POINT ( 'NONE', #71505 ) ;
#73501=ORIENTED_EDGE ( 'NONE', *, *, #46456, .T. ) ;
#73505=CARTESIAN_POINT ( 'NONE',  ( 0.000000000000000000, 0.000000000000000000, -1.466666666666671670 ) ) ;
#73591=( NAMED_UNIT ( * ) PLANE_ANGLE_UNIT ( ) SI_UNIT ( $, .RADIAN. ) );
#73740=ORIENTED_EDGE ( 'NONE', *, *, #6715, .F. ) ;
#73858=VERTEX_POINT ( 'NONE', #38235 ) ;
#73921=DIRECTION ( 'NONE',  ( -0.000000000000000000, -0.000000000000000000, -1.000000000000000000 ) ) ;
#73928=VECTOR ( 'NONE', #34613, 1000.000000000000114 ) ;
#74008=SURFACE_STYLE_USAGE ( .BOTH. , #68009 ) ;
#74036=FACE_OUTER_BOUND ( 'NONE', #11132, .T. ) ;
#74250=LINE ( 'NONE', #4747, #49912 ) ;
#74315=AXIS2_PLACEMENT_3D ( 'NONE', #16084, #26980, #4085 ) ;
ENDSEC;
END-ISO-10303-21;
